ISO-10303-21;
HEADER;
/* Generated by software containing ST-Developer
 * from STEP Tools, Inc. (www.steptools.com) 
 */

FILE_DESCRIPTION(
/* description */ ('Hand drill press frame (manual)'),
/* implementation_level */ '2;1');

FILE_NAME(
/* name */ 'M4x10 Cap Screw.step',
/* time_stamp */ '2026-10-28T03:25:28-07:00',
/* author */ (''),
/* organization */ (''),
/* preprocessor_version */ 'ST-DEVELOPER v20.2',
/* originating_system */ 'Autodesk Translation Framework v15.17.0.0',
/* authorisation */ '');

FILE_SCHEMA (('AUTOMOTIVE_DESIGN { 1 0 10303 214 3 1 1 }'));
ENDSEC;

DATA;
#10=MECHANICAL_DESIGN_GEOMETRIC_PRESENTATION_REPRESENTATION('',(#648),#33299);
#131=ORIENTED_CLOSED_SHELL('',*,#12666,.F.);
#134=BREP_WITH_VOIDS('Body1',#12667,(#131));
#478=CONICAL_SURFACE('',#13744,0.325,0.785398163397448);
#479=CONICAL_SURFACE('',#13748,0.335,0.785398163397448);
#480=CONICAL_SURFACE('',#13752,0.21,0.463647609000806);
#551=SHAPE_REPRESENTATION_RELATIONSHIP('SRR','None',#33511,#596);
#596=ADVANCED_BREP_SHAPE_REPRESENTATION('',(#134),#33273);
#648=STYLED_ITEM('',(#33821),#134);
#845=FACE_BOUND('',#2432,.T.);
#1033=PLANE('',#13732);
#1034=PLANE('',#13733);
#1035=PLANE('',#13734);
#1036=PLANE('',#13735);
#1037=PLANE('',#13736);
#1038=PLANE('',#13737);
#1039=PLANE('',#13738);
#1040=PLANE('',#13739);
#1041=PLANE('',#13740);
#1042=PLANE('',#13742);
#1043=PLANE('',#13750);
#1604=FACE_OUTER_BOUND('',#2418,.T.);
#1605=FACE_OUTER_BOUND('',#2419,.T.);
#1606=FACE_OUTER_BOUND('',#2420,.T.);
#1607=FACE_OUTER_BOUND('',#2421,.T.);
#1608=FACE_OUTER_BOUND('',#2422,.T.);
#1609=FACE_OUTER_BOUND('',#2423,.T.);
#1610=FACE_OUTER_BOUND('',#2424,.T.);
#1611=FACE_OUTER_BOUND('',#2425,.T.);
#1612=FACE_OUTER_BOUND('',#2426,.T.);
#1613=FACE_OUTER_BOUND('',#2427,.T.);
#1614=FACE_OUTER_BOUND('',#2428,.T.);
#1615=FACE_OUTER_BOUND('',#2429,.T.);
#1616=FACE_OUTER_BOUND('',#2430,.T.);
#1617=FACE_OUTER_BOUND('',#2431,.T.);
#1618=FACE_OUTER_BOUND('',#2433,.T.);
#1619=FACE_OUTER_BOUND('',#2434,.T.);
#2418=EDGE_LOOP('',(#9645,#9646,#9647,#9648));
#2419=EDGE_LOOP('',(#9649,#9650,#9651,#9652));
#2420=EDGE_LOOP('',(#9653,#9654,#9655,#9656));
#2421=EDGE_LOOP('',(#9657,#9658,#9659,#9660));
#2422=EDGE_LOOP('',(#9661,#9662,#9663,#9664));
#2423=EDGE_LOOP('',(#9665,#9666,#9667,#9668));
#2424=EDGE_LOOP('',(#9669,#9670,#9671,#9672,#9673,#9674));
#2425=EDGE_LOOP('',(#9675,#9676,#9677,#9678,#9679,#9680));
#2426=EDGE_LOOP('',(#9681));
#2427=EDGE_LOOP('',(#9682));
#2428=EDGE_LOOP('',(#9683,#9684,#9685,#9686));
#2429=EDGE_LOOP('',(#9687,#9688,#9689,#9690));
#2430=EDGE_LOOP('',(#9691,#9692,#9693,#9694));
#2431=EDGE_LOOP('',(#9695));
#2432=EDGE_LOOP('',(#9696));
#2433=EDGE_LOOP('',(#9697,#9698,#9699,#9700));
#2434=EDGE_LOOP('',(#9701,#9702,#9703,#9704));
#3219=LINE('',#19694,#4384);
#3220=LINE('',#19696,#4385);
#3221=LINE('',#19698,#4386);
#3222=LINE('',#19699,#4387);
#3223=LINE('',#19702,#4388);
#3224=LINE('',#19704,#4389);
#3225=LINE('',#19705,#4390);
#3226=LINE('',#19708,#4391);
#3227=LINE('',#19710,#4392);
#3228=LINE('',#19711,#4393);
#3229=LINE('',#19714,#4394);
#3230=LINE('',#19716,#4395);
#3231=LINE('',#19717,#4396);
#3232=LINE('',#19720,#4397);
#3233=LINE('',#19722,#4398);
#3234=LINE('',#19723,#4399);
#3235=LINE('',#19725,#4400);
#3236=LINE('',#19726,#4401);
#3237=LINE('',#19738,#4402);
#3238=LINE('',#19742,#4403);
#3239=LINE('',#19746,#4404);
#3240=LINE('',#19753,#4405);
#3241=LINE('',#19755,#4406);
#4384=VECTOR('',#15792,1.);
#4385=VECTOR('',#15793,1.);
#4386=VECTOR('',#15794,1.);
#4387=VECTOR('',#15795,1.);
#4388=VECTOR('',#15798,1.);
#4389=VECTOR('',#15799,1.);
#4390=VECTOR('',#15800,1.);
#4391=VECTOR('',#15803,1.);
#4392=VECTOR('',#15804,1.);
#4393=VECTOR('',#15805,1.);
#4394=VECTOR('',#15808,1.);
#4395=VECTOR('',#15809,1.);
#4396=VECTOR('',#15810,1.);
#4397=VECTOR('',#15813,1.);
#4398=VECTOR('',#15814,1.);
#4399=VECTOR('',#15815,1.);
#4400=VECTOR('',#15818,1.);
#4401=VECTOR('',#15819,1.);
#4402=VECTOR('',#15836,0.325);
#4403=VECTOR('',#15841,0.35);
#4404=VECTOR('',#15846,0.335);
#4405=VECTOR('',#15855,0.21);
#4406=VECTOR('',#15858,0.2);
#5462=CIRCLE('',#13741,0.1954);
#5463=CIRCLE('',#13743,0.3);
#5464=CIRCLE('',#13745,0.35);
#5465=CIRCLE('',#13747,0.35);
#5466=CIRCLE('',#13749,0.32);
#5467=CIRCLE('',#13751,0.22);
#5468=CIRCLE('',#13753,0.1954);
#6029=VERTEX_POINT('',#19692);
#6030=VERTEX_POINT('',#19693);
#6031=VERTEX_POINT('',#19695);
#6032=VERTEX_POINT('',#19697);
#6033=VERTEX_POINT('',#19701);
#6034=VERTEX_POINT('',#19703);
#6035=VERTEX_POINT('',#19707);
#6036=VERTEX_POINT('',#19709);
#6037=VERTEX_POINT('',#19713);
#6038=VERTEX_POINT('',#19715);
#6039=VERTEX_POINT('',#19719);
#6040=VERTEX_POINT('',#19721);
#6041=VERTEX_POINT('',#19730);
#6042=VERTEX_POINT('',#19733);
#6043=VERTEX_POINT('',#19736);
#6044=VERTEX_POINT('',#19740);
#6045=VERTEX_POINT('',#19744);
#6046=VERTEX_POINT('',#19748);
#6047=VERTEX_POINT('',#19751);
#7351=EDGE_CURVE('',#6029,#6030,#3219,.T.);
#7352=EDGE_CURVE('',#6030,#6031,#3220,.T.);
#7353=EDGE_CURVE('',#6031,#6032,#3221,.T.);
#7354=EDGE_CURVE('',#6029,#6032,#3222,.T.);
#7355=EDGE_CURVE('',#6030,#6033,#3223,.T.);
#7356=EDGE_CURVE('',#6033,#6034,#3224,.T.);
#7357=EDGE_CURVE('',#6034,#6031,#3225,.T.);
#7358=EDGE_CURVE('',#6033,#6035,#3226,.T.);
#7359=EDGE_CURVE('',#6035,#6036,#3227,.T.);
#7360=EDGE_CURVE('',#6036,#6034,#3228,.T.);
#7361=EDGE_CURVE('',#6035,#6037,#3229,.T.);
#7362=EDGE_CURVE('',#6037,#6038,#3230,.T.);
#7363=EDGE_CURVE('',#6038,#6036,#3231,.T.);
#7364=EDGE_CURVE('',#6037,#6039,#3232,.T.);
#7365=EDGE_CURVE('',#6039,#6040,#3233,.T.);
#7366=EDGE_CURVE('',#6040,#6038,#3234,.T.);
#7367=EDGE_CURVE('',#6039,#6029,#3235,.T.);
#7368=EDGE_CURVE('',#6032,#6040,#3236,.T.);
#7369=EDGE_CURVE('',#6041,#6041,#5462,.T.);
#7370=EDGE_CURVE('',#6042,#6042,#5463,.T.);
#7371=EDGE_CURVE('',#6043,#6043,#5464,.T.);
#7372=EDGE_CURVE('',#6043,#6042,#3237,.T.);
#7373=EDGE_CURVE('',#6044,#6044,#5465,.T.);
#7374=EDGE_CURVE('',#6044,#6043,#3238,.T.);
#7375=EDGE_CURVE('',#6045,#6045,#5466,.T.);
#7376=EDGE_CURVE('',#6045,#6044,#3239,.T.);
#7377=EDGE_CURVE('',#6046,#6046,#5467,.T.);
#7378=EDGE_CURVE('',#6047,#6047,#5468,.F.);
#7379=EDGE_CURVE('',#6047,#6046,#3240,.T.);
#7380=EDGE_CURVE('',#6041,#6047,#3241,.T.);
#9645=ORIENTED_EDGE('',*,*,#7351,.T.);
#9646=ORIENTED_EDGE('',*,*,#7352,.T.);
#9647=ORIENTED_EDGE('',*,*,#7353,.T.);
#9648=ORIENTED_EDGE('',*,*,#7354,.F.);
#9649=ORIENTED_EDGE('',*,*,#7355,.T.);
#9650=ORIENTED_EDGE('',*,*,#7356,.T.);
#9651=ORIENTED_EDGE('',*,*,#7357,.T.);
#9652=ORIENTED_EDGE('',*,*,#7352,.F.);
#9653=ORIENTED_EDGE('',*,*,#7358,.T.);
#9654=ORIENTED_EDGE('',*,*,#7359,.T.);
#9655=ORIENTED_EDGE('',*,*,#7360,.T.);
#9656=ORIENTED_EDGE('',*,*,#7356,.F.);
#9657=ORIENTED_EDGE('',*,*,#7361,.T.);
#9658=ORIENTED_EDGE('',*,*,#7362,.T.);
#9659=ORIENTED_EDGE('',*,*,#7363,.T.);
#9660=ORIENTED_EDGE('',*,*,#7359,.F.);
#9661=ORIENTED_EDGE('',*,*,#7364,.T.);
#9662=ORIENTED_EDGE('',*,*,#7365,.T.);
#9663=ORIENTED_EDGE('',*,*,#7366,.T.);
#9664=ORIENTED_EDGE('',*,*,#7362,.F.);
#9665=ORIENTED_EDGE('',*,*,#7367,.T.);
#9666=ORIENTED_EDGE('',*,*,#7354,.T.);
#9667=ORIENTED_EDGE('',*,*,#7368,.T.);
#9668=ORIENTED_EDGE('',*,*,#7365,.F.);
#9669=ORIENTED_EDGE('',*,*,#7367,.F.);
#9670=ORIENTED_EDGE('',*,*,#7364,.F.);
#9671=ORIENTED_EDGE('',*,*,#7361,.F.);
#9672=ORIENTED_EDGE('',*,*,#7358,.F.);
#9673=ORIENTED_EDGE('',*,*,#7355,.F.);
#9674=ORIENTED_EDGE('',*,*,#7351,.F.);
#9675=ORIENTED_EDGE('',*,*,#7368,.F.);
#9676=ORIENTED_EDGE('',*,*,#7353,.F.);
#9677=ORIENTED_EDGE('',*,*,#7357,.F.);
#9678=ORIENTED_EDGE('',*,*,#7360,.F.);
#9679=ORIENTED_EDGE('',*,*,#7363,.F.);
#9680=ORIENTED_EDGE('',*,*,#7366,.F.);
#9681=ORIENTED_EDGE('',*,*,#7369,.F.);
#9682=ORIENTED_EDGE('',*,*,#7370,.F.);
#9683=ORIENTED_EDGE('',*,*,#7371,.F.);
#9684=ORIENTED_EDGE('',*,*,#7372,.T.);
#9685=ORIENTED_EDGE('',*,*,#7370,.T.);
#9686=ORIENTED_EDGE('',*,*,#7372,.F.);
#9687=ORIENTED_EDGE('',*,*,#7373,.F.);
#9688=ORIENTED_EDGE('',*,*,#7374,.T.);
#9689=ORIENTED_EDGE('',*,*,#7371,.T.);
#9690=ORIENTED_EDGE('',*,*,#7374,.F.);
#9691=ORIENTED_EDGE('',*,*,#7375,.F.);
#9692=ORIENTED_EDGE('',*,*,#7376,.T.);
#9693=ORIENTED_EDGE('',*,*,#7373,.T.);
#9694=ORIENTED_EDGE('',*,*,#7376,.F.);
#9695=ORIENTED_EDGE('',*,*,#7375,.T.);
#9696=ORIENTED_EDGE('',*,*,#7377,.F.);
#9697=ORIENTED_EDGE('',*,*,#7378,.F.);
#9698=ORIENTED_EDGE('',*,*,#7379,.T.);
#9699=ORIENTED_EDGE('',*,*,#7377,.T.);
#9700=ORIENTED_EDGE('',*,*,#7379,.F.);
#9701=ORIENTED_EDGE('',*,*,#7369,.T.);
#9702=ORIENTED_EDGE('',*,*,#7380,.T.);
#9703=ORIENTED_EDGE('',*,*,#7378,.T.);
#9704=ORIENTED_EDGE('',*,*,#7380,.F.);
#11883=CYLINDRICAL_SURFACE('',#13746,0.35);
#11884=CYLINDRICAL_SURFACE('',#13754,0.1954);
#12213=ADVANCED_FACE('',(#1604),#1033,.F.);
#12214=ADVANCED_FACE('',(#1605),#1034,.F.);
#12215=ADVANCED_FACE('',(#1606),#1035,.F.);
#12216=ADVANCED_FACE('',(#1607),#1036,.F.);
#12217=ADVANCED_FACE('',(#1608),#1037,.F.);
#12218=ADVANCED_FACE('',(#1609),#1038,.F.);
#12219=ADVANCED_FACE('',(#1610),#1039,.F.);
#12220=ADVANCED_FACE('',(#1611),#1040,.F.);
#12221=ADVANCED_FACE('',(#1612),#1041,.F.);
#12222=ADVANCED_FACE('',(#1613),#1042,.T.);
#12223=ADVANCED_FACE('',(#1614),#478,.T.);
#12224=ADVANCED_FACE('',(#1615),#11883,.T.);
#12225=ADVANCED_FACE('',(#1616),#479,.T.);
#12226=ADVANCED_FACE('',(#1617,#845),#1043,.T.);
#12227=ADVANCED_FACE('',(#1618),#480,.T.);
#12228=ADVANCED_FACE('',(#1619),#11884,.T.);
#12666=CLOSED_SHELL('',(#12213,#12214,#12215,#12216,#12217,#12218,#12219,
#12220));
#12667=CLOSED_SHELL('',(#12221,#12222,#12223,#12224,#12225,#12226,#12227,
#12228));
#13731=AXIS2_PLACEMENT_3D('',#19690,#15788,#15789);
#13732=AXIS2_PLACEMENT_3D('',#19691,#15790,#15791);
#13733=AXIS2_PLACEMENT_3D('',#19700,#15796,#15797);
#13734=AXIS2_PLACEMENT_3D('',#19706,#15801,#15802);
#13735=AXIS2_PLACEMENT_3D('',#19712,#15806,#15807);
#13736=AXIS2_PLACEMENT_3D('',#19718,#15811,#15812);
#13737=AXIS2_PLACEMENT_3D('',#19724,#15816,#15817);
#13738=AXIS2_PLACEMENT_3D('',#19727,#15820,#15821);
#13739=AXIS2_PLACEMENT_3D('',#19728,#15822,#15823);
#13740=AXIS2_PLACEMENT_3D('',#19729,#15824,#15825);
#13741=AXIS2_PLACEMENT_3D('',#19731,#15826,#15827);
#13742=AXIS2_PLACEMENT_3D('',#19732,#15828,#15829);
#13743=AXIS2_PLACEMENT_3D('',#19734,#15830,#15831);
#13744=AXIS2_PLACEMENT_3D('',#19735,#15832,#15833);
#13745=AXIS2_PLACEMENT_3D('',#19737,#15834,#15835);
#13746=AXIS2_PLACEMENT_3D('',#19739,#15837,#15838);
#13747=AXIS2_PLACEMENT_3D('',#19741,#15839,#15840);
#13748=AXIS2_PLACEMENT_3D('',#19743,#15842,#15843);
#13749=AXIS2_PLACEMENT_3D('',#19745,#15844,#15845);
#13750=AXIS2_PLACEMENT_3D('',#19747,#15847,#15848);
#13751=AXIS2_PLACEMENT_3D('',#19749,#15849,#15850);
#13752=AXIS2_PLACEMENT_3D('',#19750,#15851,#15852);
#13753=AXIS2_PLACEMENT_3D('',#19752,#15853,#15854);
#13754=AXIS2_PLACEMENT_3D('',#19754,#15856,#15857);
#15788=DIRECTION('axis',(0.,0.,1.));
#15789=DIRECTION('refdir',(1.,0.,0.));
#15790=DIRECTION('center_axis',(0.866025403784439,0.,-0.5));
#15791=DIRECTION('ref_axis',(0.5,0.,0.866025403784439));
#15792=DIRECTION('',(-0.5,0.,-0.866025403784439));
#15793=DIRECTION('',(0.,-1.,0.));
#15794=DIRECTION('',(0.5,0.,0.866025403784439));
#15795=DIRECTION('',(0.,-1.,0.));
#15796=DIRECTION('center_axis',(1.60246890531964E-16,0.,-1.));
#15797=DIRECTION('ref_axis',(1.,0.,1.60246890531964E-16));
#15798=DIRECTION('',(-1.,0.,-1.60246890531964E-16));
#15799=DIRECTION('',(0.,-1.,0.));
#15800=DIRECTION('',(1.,0.,1.60246890531964E-16));
#15801=DIRECTION('center_axis',(-0.866025403784439,0.,-0.5));
#15802=DIRECTION('ref_axis',(0.5,0.,-0.866025403784439));
#15803=DIRECTION('',(-0.5,0.,0.866025403784439));
#15804=DIRECTION('',(0.,-1.,0.));
#15805=DIRECTION('',(0.5,0.,-0.866025403784439));
#15806=DIRECTION('center_axis',(-0.866025403784439,0.,0.5));
#15807=DIRECTION('ref_axis',(-0.5,0.,-0.866025403784439));
#15808=DIRECTION('',(0.5,0.,0.866025403784439));
#15809=DIRECTION('',(0.,-1.,0.));
#15810=DIRECTION('',(-0.5,0.,-0.866025403784439));
#15811=DIRECTION('center_axis',(-1.60246890531964E-16,0.,1.));
#15812=DIRECTION('ref_axis',(-1.,0.,-1.60246890531964E-16));
#15813=DIRECTION('',(1.,0.,1.60246890531964E-16));
#15814=DIRECTION('',(0.,-1.,0.));
#15815=DIRECTION('',(-1.,0.,-1.60246890531964E-16));
#15816=DIRECTION('center_axis',(0.866025403784439,0.,0.5));
#15817=DIRECTION('ref_axis',(-0.5,0.,0.866025403784439));
#15818=DIRECTION('',(0.5,0.,-0.866025403784439));
#15819=DIRECTION('',(-0.5,0.,0.866025403784439));
#15820=DIRECTION('center_axis',(0.,1.,0.));
#15821=DIRECTION('ref_axis',(1.,0.,0.));
#15822=DIRECTION('center_axis',(0.,-1.,0.));
#15823=DIRECTION('ref_axis',(0.,0.,-1.));
#15824=DIRECTION('center_axis',(0.,1.,0.));
#15825=DIRECTION('ref_axis',(1.,0.,0.));
#15826=DIRECTION('center_axis',(0.,1.,0.));
#15827=DIRECTION('ref_axis',(1.,0.,0.));
#15828=DIRECTION('center_axis',(0.,1.,0.));
#15829=DIRECTION('ref_axis',(0.,0.,1.));
#15830=DIRECTION('center_axis',(0.,-1.,0.));
#15831=DIRECTION('ref_axis',(1.,0.,0.));
#15832=DIRECTION('center_axis',(0.,-1.,0.));
#15833=DIRECTION('ref_axis',(1.,0.,0.));
#15834=DIRECTION('center_axis',(0.,-1.,0.));
#15835=DIRECTION('ref_axis',(1.,0.,0.));
#15836=DIRECTION('',(0.707106781186547,0.707106781186548,8.65956056235493E-17));
#15837=DIRECTION('center_axis',(0.,-1.,0.));
#15838=DIRECTION('ref_axis',(1.,0.,0.));
#15839=DIRECTION('center_axis',(0.,-1.,0.));
#15840=DIRECTION('ref_axis',(1.,0.,0.));
#15841=DIRECTION('',(0.,1.,0.));
#15842=DIRECTION('center_axis',(0.,1.,0.));
#15843=DIRECTION('ref_axis',(1.,0.,0.));
#15844=DIRECTION('center_axis',(0.,-1.,0.));
#15845=DIRECTION('ref_axis',(1.,0.,0.));
#15846=DIRECTION('',(-0.707106781186547,0.707106781186548,-8.65956056235493E-17));
#15847=DIRECTION('center_axis',(0.,-1.,0.));
#15848=DIRECTION('ref_axis',(0.,0.,-1.));
#15849=DIRECTION('center_axis',(0.,-1.,0.));
#15850=DIRECTION('ref_axis',(1.,0.,0.));
#15851=DIRECTION('center_axis',(0.,1.,0.));
#15852=DIRECTION('ref_axis',(1.,0.,0.));
#15853=DIRECTION('center_axis',(0.,1.,0.));
#15854=DIRECTION('ref_axis',(1.,0.,0.));
#15855=DIRECTION('',(-0.447213595499958,0.894427190999916,-5.47678698264203E-17));
#15856=DIRECTION('center_axis',(0.,-1.,0.));
#15857=DIRECTION('ref_axis',(1.,0.,0.));
#15858=DIRECTION('',(0.,1.,0.));
#19690=CARTESIAN_POINT('',(0.,0.,0.));
#19691=CARTESIAN_POINT('Origin',(0.0866025403784439,-0.4,-0.15));
#19692=CARTESIAN_POINT('',(0.173205080756888,-0.4,0.));
#19693=CARTESIAN_POINT('',(0.0866025403784439,-0.4,-0.15));
#19694=CARTESIAN_POINT('',(0.173205080756888,-0.4,0.));
#19695=CARTESIAN_POINT('',(0.0866025403784439,-0.64,-0.15));
#19696=CARTESIAN_POINT('',(0.0866025403784439,-0.4,-0.15));
#19697=CARTESIAN_POINT('',(0.173205080756888,-0.64,0.));
#19698=CARTESIAN_POINT('',(0.173205080756888,-0.64,0.));
#19699=CARTESIAN_POINT('',(0.173205080756888,-0.4,0.));
#19700=CARTESIAN_POINT('Origin',(-0.0866025403784438,-0.4,-0.15));
#19701=CARTESIAN_POINT('',(-0.0866025403784438,-0.4,-0.15));
#19702=CARTESIAN_POINT('',(0.0866025403784439,-0.4,-0.15));
#19703=CARTESIAN_POINT('',(-0.0866025403784438,-0.64,-0.15));
#19704=CARTESIAN_POINT('',(-0.0866025403784438,-0.4,-0.15));
#19705=CARTESIAN_POINT('',(0.0866025403784439,-0.64,-0.15));
#19706=CARTESIAN_POINT('Origin',(-0.173205080756888,-0.4,-2.77555756156289E-17));
#19707=CARTESIAN_POINT('',(-0.173205080756888,-0.4,-2.12115047744981E-17));
#19708=CARTESIAN_POINT('',(-0.0866025403784438,-0.4,-0.15));
#19709=CARTESIAN_POINT('',(-0.173205080756888,-0.64,-2.77555756156289E-17));
#19710=CARTESIAN_POINT('',(-0.173205080756888,-0.4,-2.12115047744981E-17));
#19711=CARTESIAN_POINT('',(-0.0866025403784438,-0.64,-0.15));
#19712=CARTESIAN_POINT('Origin',(-0.0866025403784439,-0.4,0.15));
#19713=CARTESIAN_POINT('',(-0.0866025403784439,-0.4,0.15));
#19714=CARTESIAN_POINT('',(-0.173205080756888,-0.4,-2.12115047744981E-17));
#19715=CARTESIAN_POINT('',(-0.0866025403784439,-0.64,0.15));
#19716=CARTESIAN_POINT('',(-0.0866025403784439,-0.4,0.15));
#19717=CARTESIAN_POINT('',(-0.173205080756888,-0.64,-2.12115047744981E-17));
#19718=CARTESIAN_POINT('Origin',(0.0866025403784439,-0.4,0.15));
#19719=CARTESIAN_POINT('',(0.0866025403784439,-0.4,0.15));
#19720=CARTESIAN_POINT('',(-0.0866025403784439,-0.4,0.15));
#19721=CARTESIAN_POINT('',(0.0866025403784439,-0.64,0.15));
#19722=CARTESIAN_POINT('',(0.0866025403784439,-0.4,0.15));
#19723=CARTESIAN_POINT('',(-0.0866025403784439,-0.64,0.15));
#19724=CARTESIAN_POINT('Origin',(0.173205080756888,-0.4,0.));
#19725=CARTESIAN_POINT('',(0.0866025403784439,-0.4,0.15));
#19726=CARTESIAN_POINT('',(0.0866025403784439,-0.64,0.15));
#19727=CARTESIAN_POINT('Origin',(0.,-0.4,-2.77555756156289E-17));
#19728=CARTESIAN_POINT('Origin',(0.,-0.64,-2.77555756156289E-17));
#19729=CARTESIAN_POINT('Origin',(0.,-1.,0.));
#19730=CARTESIAN_POINT('',(-0.1954,-1.,2.39295984553393E-17));
#19731=CARTESIAN_POINT('Origin',(0.,-1.,0.));
#19732=CARTESIAN_POINT('Origin',(0.3,0.4,0.));
#19733=CARTESIAN_POINT('',(-0.3,0.4,-3.67394039744206E-17));
#19734=CARTESIAN_POINT('Origin',(0.,0.4,0.));
#19735=CARTESIAN_POINT('Origin',(0.,0.375,0.));
#19736=CARTESIAN_POINT('',(-0.35,0.35,-4.28626379701573E-17));
#19737=CARTESIAN_POINT('Origin',(0.,0.35,0.));
#19738=CARTESIAN_POINT('',(-0.325,0.375,-3.9801020972289E-17));
#19739=CARTESIAN_POINT('Origin',(0.,0.19,0.));
#19740=CARTESIAN_POINT('',(-0.35,0.03,-4.28626379701574E-17));
#19741=CARTESIAN_POINT('Origin',(0.,0.03,0.));
#19742=CARTESIAN_POINT('',(-0.35,0.19,-4.28626379701574E-17));
#19743=CARTESIAN_POINT('Origin',(0.,0.0149999999999999,0.));
#19744=CARTESIAN_POINT('',(-0.32,-3.29597460435593E-17,-3.91886975727153E-17));
#19745=CARTESIAN_POINT('Origin',(0.,0.,0.));
#19746=CARTESIAN_POINT('',(-0.335,0.0149999999999999,-4.10256677714363E-17));
#19747=CARTESIAN_POINT('Origin',(0.22,0.,0.));
#19748=CARTESIAN_POINT('',(-0.22,-6.93889390390723E-18,-2.69422295812418E-17));
#19749=CARTESIAN_POINT('Origin',(0.,0.,0.));
#19750=CARTESIAN_POINT('Origin',(0.,-0.02,0.));
#19751=CARTESIAN_POINT('',(-0.1954,-0.0492,2.39295984553393E-17));
#19752=CARTESIAN_POINT('Origin',(0.,-0.0492,0.));
#19753=CARTESIAN_POINT('',(-0.21,-0.02,-2.57175827820944E-17));
#19754=CARTESIAN_POINT('Origin',(0.,-0.8,0.));
#19755=CARTESIAN_POINT('',(-0.1954,-0.8,-2.39295984553393E-17));
#33221=UNCERTAINTY_MEASURE_WITH_UNIT(LENGTH_MEASURE(0.001),#33300,
'DISTANCE_ACCURACY_VALUE',
'Maximum model space distance between geometric entities at asserted c
onnectivities');
#33247=UNCERTAINTY_MEASURE_WITH_UNIT(LENGTH_MEASURE(0.001),#33300,
'DISTANCE_ACCURACY_VALUE',
'Maximum model space distance between geometric entities at asserted c
onnectivities');
#33273=(
GEOMETRIC_REPRESENTATION_CONTEXT(3)
GLOBAL_UNCERTAINTY_ASSIGNED_CONTEXT((#33221))
GLOBAL_UNIT_ASSIGNED_CONTEXT((#33300,#33302,#33303))
REPRESENTATION_CONTEXT('','3D')
);
#33299=(
GEOMETRIC_REPRESENTATION_CONTEXT(3)
GLOBAL_UNCERTAINTY_ASSIGNED_CONTEXT((#33247))
GLOBAL_UNIT_ASSIGNED_CONTEXT((#33300,#33302,#33303))
REPRESENTATION_CONTEXT('','3D')
);
#33300=(
LENGTH_UNIT()
NAMED_UNIT(*)
SI_UNIT(.CENTI.,.METRE.)
);
#33302=(
NAMED_UNIT(*)
PLANE_ANGLE_UNIT()
SI_UNIT($,.RADIAN.)
);
#33303=(
NAMED_UNIT(*)
SI_UNIT($,.STERADIAN.)
SOLID_ANGLE_UNIT()
);
#33329=SHAPE_DEFINITION_REPRESENTATION(#33385,#33511);
#33385=PRODUCT_DEFINITION_SHAPE('',$,#33563);
#33511=SHAPE_REPRESENTATION('',(#13731),#33273);
#33537=PRODUCT_DEFINITION_CONTEXT('part definition',#33692,'design');
#33563=PRODUCT_DEFINITION('M4x10 Cap Screw','M4x10 Cap Screw',#33614,#33537);
#33614=PRODUCT_DEFINITION_FORMATION('',$,#33719);
#33692=APPLICATION_CONTEXT(
'Core Data for Automotive Mechanical Design Process');
#33693=PRODUCT_CONTEXT('part definition',#33692,'mechanical');
#33719=PRODUCT('M4x10 Cap Screw','M4x10 Cap Screw','M4x10 Cap Screw',(#33693));
#33815=COLOUR_RGB('Black',0.12,0.14,0.17);
#33816=FILL_AREA_STYLE_COLOUR('',#33815);
#33817=FILL_AREA_STYLE('',(#33816));
#33818=SURFACE_STYLE_FILL_AREA(#33817);
#33819=SURFACE_SIDE_STYLE('',(#33818));
#33820=SURFACE_STYLE_USAGE(.BOTH.,#33819);
#33821=PRESENTATION_STYLE_ASSIGNMENT((#33820));
ENDSEC;
END-ISO-10303-21;
